ISO-10303-21;
HEADER;
FILE_DESCRIPTION (('STEP AP214'),
    '1' );
FILE_NAME ('Rotary Faceplate.step',
    '2026-10-07T17:53:07',
    ( '' ),
    ( '' ),
    'SwSTEP 2.0',
    'SolidWorks 2025',
    '' );
FILE_SCHEMA (( 'AUTOMOTIVE_DESIGN' ));
ENDSEC;

DATA;
#1=VERTEX_POINT ( 'NONE', #2797 ) ;
#13=DIRECTION ( 'NONE',  ( 0.000000000000000000, 0.000000000000000000, 1.000000000000000000 ) ) ;
#32=VECTOR ( 'NONE', #959, 1000.000000000000000 ) ;
#36=EDGE_CURVE ( 'NONE', #826, #10489, #4183, .T. ) ;
#51=VERTEX_POINT ( 'NONE', #6255 ) ;
#120=CARTESIAN_POINT ( 'NONE',  ( 0.000000000000000000, 0.000000000000000000, 0.000000000000000000 ) ) ;
#146=ORIENTED_EDGE ( 'NONE', *, *, #5230, .T. ) ;
#184=DIRECTION ( 'NONE',  ( 0.000000000000000000, 0.000000000000000000, 1.000000000000000000 ) ) ;
#189=VERTEX_POINT ( 'NONE', #4908 ) ;
#191=CARTESIAN_POINT ( 'NONE',  ( 0.000000000000000000, 0.000000000000000000, 7.000000000000000000 ) ) ;
#220=ORIENTED_EDGE ( 'NONE', *, *, #13475, .F. ) ;
#249=ORIENTED_EDGE ( 'NONE', *, *, #1249, .F. ) ;
#253=CARTESIAN_POINT ( 'NONE',  ( 0.000000000000000000, 0.000000000000000000, 7.000000000000000000 ) ) ;
#255=( GEOMETRIC_REPRESENTATION_CONTEXT ( 3 ) GLOBAL_UNCERTAINTY_ASSIGNED_CONTEXT ( ( #9779 ) ) GLOBAL_UNIT_ASSIGNED_CONTEXT ( ( #8310, #2817, #5089 ) ) REPRESENTATION_CONTEXT ( 'NONE', 'WORKASPACE' ) );
#258=ORIENTED_EDGE ( 'NONE', *, *, #1830, .F. ) ;
#286=AXIS2_PLACEMENT_3D ( 'NONE', #2851, #528, #4856 ) ;
#295=CIRCLE ( 'NONE', #286, 24.03999999999999915 ) ;
#298=ORIENTED_EDGE ( 'NONE', *, *, #13475, .T. ) ;
#303=EDGE_LOOP ( 'NONE', ( #9142, #9637, #13068, #4588 ) ) ;
#329=DIRECTION ( 'NONE',  ( -0.000000000000000000, -0.000000000000000000, -1.000000000000000000 ) ) ;
#353=ORIENTED_EDGE ( 'NONE', *, *, #4353, .F. ) ;
#356=DIRECTION ( 'NONE',  ( 1.000000000000000000, 0.000000000000000000, 0.000000000000000000 ) ) ;
#359=CYLINDRICAL_SURFACE ( 'NONE', #10271, 1.999999999999995781 ) ;
#381=EDGE_CURVE ( 'NONE', #10270, #2929, #13691, .T. ) ;
#396=DIRECTION ( 'NONE',  ( 0.000000000000000000, 0.000000000000000000, 1.000000000000000000 ) ) ;
#442=CARTESIAN_POINT ( 'NONE',  ( 10.81426999815522549, -15.06602133594279991, -3.000000000000000000 ) ) ;
#492=ADVANCED_FACE ( 'NONE', ( #5580 ), #11804, .F. ) ;
#513=FACE_BOUND ( 'NONE', #6731, .T. ) ;
#517=AXIS2_PLACEMENT_3D ( 'NONE', #13650, #944, #11756 ) ;
#528=DIRECTION ( 'NONE',  ( 0.000000000000000000, 0.000000000000000000, 1.000000000000000000 ) ) ;
#562=EDGE_CURVE ( 'NONE', #8669, #10489, #2680, .T. ) ;
#566=PRODUCT_DEFINITION ( 'UNKNOWN', '', #9121, #4050 ) ;
#574=FACE_BOUND ( 'NONE', #8182, .T. ) ;
#602=ORIENTED_EDGE ( 'NONE', *, *, #381, .T. ) ;
#622=FACE_OUTER_BOUND ( 'NONE', #303, .T. ) ;
#749=CYLINDRICAL_SURFACE ( 'NONE', #1816, 1.999999999999994893 ) ;
#765=DIRECTION ( 'NONE',  ( 1.000000000000000000, 0.000000000000000000, 0.000000000000000000 ) ) ;
#775=ORIENTED_EDGE ( 'NONE', *, *, #5852, .F. ) ;
#810=DIRECTION ( 'NONE',  ( 0.000000000000000000, 0.000000000000000000, 1.000000000000000000 ) ) ;
#826=VERTEX_POINT ( 'NONE', #11517 ) ;
#867=FACE_OUTER_BOUND ( 'NONE', #7948, .T. ) ;
#944=DIRECTION ( 'NONE',  ( -0.000000000000000000, -0.000000000000000000, 1.000000000000000000 ) ) ;
#959=DIRECTION ( 'NONE',  ( -0.000000000000000000, -0.000000000000000000, 1.000000000000000000 ) ) ;
#973=VERTEX_POINT ( 'NONE', #11936 ) ;
#976=ORIENTED_EDGE ( 'NONE', *, *, #1683, .F. ) ;
#982=EDGE_CURVE ( 'NONE', #12299, #13004, #1126, .T. ) ;
#991=CARTESIAN_POINT ( 'NONE',  ( -10.81426999815532852, 15.06602133594271820, 0.000000000000000000 ) ) ;
#1012=ORIENTED_EDGE ( 'NONE', *, *, #11390, .T. ) ;
#1017=DIRECTION ( 'NONE',  ( -0.000000000000000000, -0.000000000000000000, 1.000000000000000000 ) ) ;
#1025=ORIENTED_EDGE ( 'NONE', *, *, #5478, .T. ) ;
#1040=EDGE_LOOP ( 'NONE', ( #4955, #12743 ) ) ;
#1046=DIRECTION ( 'NONE',  ( 1.000000000000000000, 0.000000000000000000, 0.000000000000000000 ) ) ;
#1048=AXIS2_PLACEMENT_3D ( 'NONE', #5562, #7652, #4535 ) ;
#1067=AXIS2_PLACEMENT_3D ( 'NONE', #6316, #6958, #11232 ) ;
#1076=VECTOR ( 'NONE', #13792, 1000.000000000000000 ) ;
#1079=ORIENTED_EDGE ( 'NONE', *, *, #4393, .F. ) ;
#1089=CARTESIAN_POINT ( 'NONE',  ( -10.81426999815532852, 15.06602133594271820, 0.000000000000000000 ) ) ;
#1126=CIRCLE ( 'NONE', #10732, 24.03999999999999915 ) ;
#1154=DIRECTION ( 'NONE',  ( 0.000000000000000000, 0.000000000000000000, 1.000000000000000000 ) ) ;
#1155=ORIENTED_EDGE ( 'NONE', *, *, #8188, .T. ) ;
#1185=LINE ( 'NONE', #9717, #10085 ) ;
#1249=EDGE_CURVE ( 'NONE', #12867, #1551, #4039, .T. ) ;
#1251=DIRECTION ( 'NONE',  ( 0.000000000000000000, 0.000000000000000000, 1.000000000000000000 ) ) ;
#1265=ORIENTED_EDGE ( 'NONE', *, *, #12420, .T. ) ;
#1268=DIRECTION ( 'NONE',  ( -0.000000000000000000, -0.000000000000000000, -1.000000000000000000 ) ) ;
#1272=LINE ( 'NONE', #2426, #4966 ) ;
#1288=DIRECTION ( 'NONE',  ( 0.000000000000000000, 0.000000000000000000, 1.000000000000000000 ) ) ;
#1302=EDGE_LOOP ( 'NONE', ( #10862, #1884 ) ) ;
#1317=CARTESIAN_POINT ( 'NONE',  ( 0.000000000000000000, 0.000000000000000000, -43.00000000000000000 ) ) ;
#1352=LINE ( 'NONE', #13083, #12495 ) ;
#1371=CIRCLE ( 'NONE', #8739, 1.999999999999996669 ) ;
#1441=AXIS2_PLACEMENT_3D ( 'NONE', #11116, #13337, #1544 ) ;
#1445=LINE ( 'NONE', #8925, #6698 ) ;
#1502=CARTESIAN_POINT ( 'NONE',  ( 0.000000000000000000, 0.000000000000000000, 7.000000000000000000 ) ) ;
#1515=DIRECTION ( 'NONE',  ( -0.000000000000000000, -0.000000000000000000, 1.000000000000000000 ) ) ;
#1532=AXIS2_PLACEMENT_3D ( 'NONE', #10626, #4480, #1046 ) ;
#1544=DIRECTION ( 'NONE',  ( 1.000000000000000000, 0.000000000000000000, 0.000000000000000000 ) ) ;
#1551=VERTEX_POINT ( 'NONE', #3458 ) ;
#1554=FACE_OUTER_BOUND ( 'NONE', #3019, .T. ) ;
#1565=VECTOR ( 'NONE', #5716, 1000.000000000000000 ) ;
#1582=ADVANCED_FACE ( 'NONE', ( #8819 ), #11065, .F. ) ;
#1592=DIRECTION ( 'NONE',  ( 1.000000000000000000, 0.000000000000000000, 0.000000000000000000 ) ) ;
#1594=CARTESIAN_POINT ( 'NONE',  ( -24.03999999999999915, 0.000000000000000000, 7.000000000000000000 ) ) ;
#1668=ORIENTED_EDGE ( 'NONE', *, *, #2700, .T. ) ;
#1672=CARTESIAN_POINT ( 'NONE',  ( 16.45469220996245241, 1.832421873814834345, 7.000000000000000000 ) ) ;
#1683=EDGE_CURVE ( 'NONE', #9990, #11639, #2703, .T. ) ;
#1689=FACE_BOUND ( 'NONE', #9516, .T. ) ;
#1693=CARTESIAN_POINT ( 'NONE',  ( 18.45469220996244886, 1.832421873814834123, 7.000000000000000000 ) ) ;
#1696=EDGE_CURVE ( 'NONE', #9008, #10592, #4507, .T. ) ;
#1711=EDGE_LOOP ( 'NONE', ( #4221, #4676, #1668, #12719 ) ) ;
#1781=ORIENTED_EDGE ( 'NONE', *, *, #9253, .F. ) ;
#1816=AXIS2_PLACEMENT_3D ( 'NONE', #11578, #12485, #7290 ) ;
#1830=EDGE_CURVE ( 'NONE', #9038, #11639, #3153, .T. ) ;
#1851=EDGE_LOOP ( 'NONE', ( #8904, #12789, #1012, #5990 ) ) ;
#1863=SHAPE_DEFINITION_REPRESENTATION ( #8638, #2236 ) ;
#1884=ORIENTED_EDGE ( 'NONE', *, *, #10411, .T. ) ;
#1896=ORIENTED_EDGE ( 'NONE', *, *, #562, .F. ) ;
#1948=EDGE_LOOP ( 'NONE', ( #8762, #258 ) ) ;
#1963=CYLINDRICAL_SURFACE ( 'NONE', #3625, 1.999999999999991340 ) ;
#1986=DIRECTION ( 'NONE',  ( 0.000000000000000000, 0.000000000000000000, 1.000000000000000000 ) ) ;
#2012=LINE ( 'NONE', #6454, #11612 ) ;
#2093=FACE_OUTER_BOUND ( 'NONE', #10375, .T. ) ;
#2108=DIRECTION ( 'NONE',  ( 1.000000000000000000, 0.000000000000000000, 0.000000000000000000 ) ) ;
#2148=ADVANCED_FACE ( 'NONE', ( #11652 ), #749, .F. ) ;
#2175=DIRECTION ( 'NONE',  ( 1.000000000000000000, 0.000000000000000000, 0.000000000000000000 ) ) ;
#2236=SHAPE_REPRESENTATION ( 'Rotary Faceplate', ( #6434 ), #2686 ) ;
#2311=EDGE_CURVE ( 'NONE', #189, #8669, #6714, .T. ) ;
#2346=ORIENTED_EDGE ( 'NONE', *, *, #5852, .T. ) ;
#2383=DIRECTION ( 'NONE',  ( 0.000000000000000000, 0.000000000000000000, 1.000000000000000000 ) ) ;
#2395=DIRECTION ( 'NONE',  ( 1.000000000000000000, 0.000000000000000000, 0.000000000000000000 ) ) ;
#2418=ORIENTED_EDGE ( 'NONE', *, *, #10599, .F. ) ;
#2426=CARTESIAN_POINT ( 'NONE',  ( -20.45469220996243820, -1.832421873814833901, -3.000000000000000000 ) ) ;
#2474=FILL_AREA_STYLE_COLOUR ( '', #6719 ) ;
#2490=VECTOR ( 'NONE', #3100, 1000.000000000000000 ) ;
#2538=ORIENTED_EDGE ( 'NONE', *, *, #7080, .T. ) ;
#2545=CARTESIAN_POINT ( 'NONE',  ( -20.45469220996243820, -1.832421873814833901, 0.000000000000000000 ) ) ;
#2547=SURFACE_STYLE_FILL_AREA ( #9930 ) ;
#2580=ADVANCED_FACE ( 'NONE', ( #7211 ), #12470, .F. ) ;
#2581=FACE_OUTER_BOUND ( 'NONE', #1851, .T. ) ;
#2617=EDGE_CURVE ( 'NONE', #12491, #3628, #13446, .T. ) ;
#2618=ORIENTED_EDGE ( 'NONE', *, *, #7381, .T. ) ;
#2640=DIRECTION ( 'NONE',  ( -0.000000000000000000, -0.000000000000000000, -1.000000000000000000 ) ) ;
#2663=DIRECTION ( 'NONE',  ( 1.000000000000000000, 0.000000000000000000, 0.000000000000000000 ) ) ;
#2666=DIRECTION ( 'NONE',  ( 0.000000000000000000, 0.000000000000000000, 1.000000000000000000 ) ) ;
#2679=AXIS2_PLACEMENT_3D ( 'NONE', #3104, #10627, #4211 ) ;
#2680=LINE ( 'NONE', #7039, #1565 ) ;
#2686=( GEOMETRIC_REPRESENTATION_CONTEXT ( 3 ) GLOBAL_UNCERTAINTY_ASSIGNED_CONTEXT ( ( #3908 ) ) GLOBAL_UNIT_ASSIGNED_CONTEXT ( ( #4660, #4526, #5830 ) ) REPRESENTATION_CONTEXT ( 'NONE', 'WORKASPACE' ) );
#2700=EDGE_CURVE ( 'NONE', #1551, #51, #1371, .T. ) ;
#2703=LINE ( 'NONE', #8756, #6946 ) ;
#2734=CYLINDRICAL_SURFACE ( 'NONE', #1067, 1.999999999999994893 ) ;
#2769=FACE_BOUND ( 'NONE', #3364, .T. ) ;
#2797=CARTESIAN_POINT ( 'NONE',  ( 12.81426999815521839, -15.06602133594279991, 7.000000000000000000 ) ) ;
#2817=( NAMED_UNIT ( * ) PLANE_ANGLE_UNIT ( ) SI_UNIT ( $, .RADIAN. ) );
#2851=CARTESIAN_POINT ( 'NONE',  ( 0.000000000000000000, 0.000000000000000000, 7.000000000000000000 ) ) ;
#2861=ORIENTED_EDGE ( 'NONE', *, *, #6604, .T. ) ;
#2865=FACE_OUTER_BOUND ( 'NONE', #9805, .T. ) ;
#2875=DIRECTION ( 'NONE',  ( 0.000000000000000000, 0.000000000000000000, 1.000000000000000000 ) ) ;
#2915=ORIENTED_EDGE ( 'NONE', *, *, #2311, .T. ) ;
#2929=VERTEX_POINT ( 'NONE', #6932 ) ;
#2934=DIRECTION ( 'NONE',  ( 0.000000000000000000, 0.000000000000000000, 1.000000000000000000 ) ) ;
#2953=ORIENTED_EDGE ( 'NONE', *, *, #5984, .F. ) ;
#2987=EDGE_CURVE ( 'NONE', #4661, #12066, #11474, .T. ) ;
#2992=EDGE_CURVE ( 'NONE', #7369, #12154, #7549, .T. ) ;
#3019=EDGE_LOOP ( 'NONE', ( #11322, #146 ) ) ;
#3022=DIRECTION ( 'NONE',  ( 1.000000000000000000, 0.000000000000000000, 0.000000000000000000 ) ) ;
#3058=CARTESIAN_POINT ( 'NONE',  ( -18.45469220996244886, -1.832421873814834123, -3.000000000000000000 ) ) ;
#3100=DIRECTION ( 'NONE',  ( -0.000000000000000000, -0.000000000000000000, 1.000000000000000000 ) ) ;
#3104=CARTESIAN_POINT ( 'NONE',  ( 7.640422211807137209, 16.89844320975774750, 0.000000000000000000 ) ) ;
#3110=VECTOR ( 'NONE', #5701, 1000.000000000000000 ) ;
#3153=CIRCLE ( 'NONE', #6480, 1.999999999999994893 ) ;
#3154=ORIENTED_EDGE ( 'NONE', *, *, #1696, .F. ) ;
#3171=EDGE_LOOP ( 'NONE', ( #9666, #6901 ) ) ;
#3185=DIRECTION ( 'NONE',  ( 1.000000000000000000, 0.000000000000000000, 0.000000000000000000 ) ) ;
#3197=CYLINDRICAL_SURFACE ( 'NONE', #517, 1.999999999999993117 ) ;
#3201=AXIS2_PLACEMENT_3D ( 'NONE', #7271, #12806, #11697 ) ;
#3217=AXIS2_PLACEMENT_3D ( 'NONE', #13051, #2666, #3495 ) ;
#3219=FACE_BOUND ( 'NONE', #1302, .T. ) ;
#3238=DIRECTION ( 'NONE',  ( -0.000000000000000000, -0.000000000000000000, 1.000000000000000000 ) ) ;
#3287=DIRECTION ( 'NONE',  ( -0.000000000000000000, -0.000000000000000000, 1.000000000000000000 ) ) ;
#3302=AXIS2_PLACEMENT_3D ( 'NONE', #253, #2640, #4517 ) ;
#3327=ADVANCED_FACE ( 'NONE', ( #10992 ), #359, .F. ) ;
#3334=DIRECTION ( 'NONE',  ( 1.000000000000000000, 0.000000000000000000, 0.000000000000000000 ) ) ;
#3364=EDGE_LOOP ( 'NONE', ( #10236, #12436 ) ) ;
#3411=LINE ( 'NONE', #11577, #1076 ) ;
#3441=DIRECTION ( 'NONE',  ( 1.000000000000000000, 0.000000000000000000, 0.000000000000000000 ) ) ;
#3458=CARTESIAN_POINT ( 'NONE',  ( 5.640422211807141650, 16.89844320975774750, 7.000000000000000000 ) ) ;
#3462=DIRECTION ( 'NONE',  ( -0.000000000000000000, -0.000000000000000000, 1.000000000000000000 ) ) ;
#3489=DIRECTION ( 'NONE',  ( 0.000000000000000000, 0.000000000000000000, 1.000000000000000000 ) ) ;
#3495=DIRECTION ( 'NONE',  ( 1.000000000000000000, 0.000000000000000000, 0.000000000000000000 ) ) ;
#3514=CARTESIAN_POINT ( 'NONE',  ( 24.03999999999999915, 2.944050905150237001E-15, 0.000000000000000000 ) ) ;
#3556=DIRECTION ( 'NONE',  ( 1.000000000000000000, 0.000000000000000000, 0.000000000000000000 ) ) ;
#3560=EDGE_LOOP ( 'NONE', ( #8901, #2915 ) ) ;
#3582=CARTESIAN_POINT ( 'NONE',  ( -10.81426999815532852, 15.06602133594271820, -3.000000000000000000 ) ) ;
#3585=DIRECTION ( 'NONE',  ( -0.000000000000000000, -0.000000000000000000, 1.000000000000000000 ) ) ;
#3624=SHAPE_REPRESENTATION_RELATIONSHIP ( 'NONE' , 'NONE' ,  #2236, #7898 ) ;
#3625=AXIS2_PLACEMENT_3D ( 'NONE', #12369, #10402, #765 ) ;
#3628=VERTEX_POINT ( 'NONE', #10972 ) ;
#3672=EDGE_CURVE ( 'NONE', #10592, #9852, #1445, .T. ) ;
#3686=DIRECTION ( 'NONE',  ( 1.000000000000000000, 0.000000000000000000, 0.000000000000000000 ) ) ;
#3709=CARTESIAN_POINT ( 'NONE',  ( 16.45469220996245241, 1.832421873814834345, 0.000000000000000000 ) ) ;
#3721=PLANE ( 'NONE',  #12515 ) ;
#3769=CIRCLE ( 'NONE', #5980, 6.000000000000000888 ) ;
#3785=AXIS2_PLACEMENT_3D ( 'NONE', #6227, #7258, #8332 ) ;
#3816=CARTESIAN_POINT ( 'NONE',  ( 6.000000000000000888, 0.000000000000000000, 7.000000000000000000 ) ) ;
#3908=UNCERTAINTY_MEASURE_WITH_UNIT (LENGTH_MEASURE( 1.000000000000000082E-05 ), #4660, 'distance_accuracy_value', 'NONE');
#3928=EDGE_LOOP ( 'NONE', ( #12987, #6253, #2618, #4889 ) ) ;
#3981=CARTESIAN_POINT ( 'NONE',  ( -20.45469220996243820, -1.832421873814833901, 7.000000000000000000 ) ) ;
#4009=DIRECTION ( 'NONE',  ( 0.000000000000000000, 0.000000000000000000, 1.000000000000000000 ) ) ;
#4011=EDGE_CURVE ( 'NONE', #12154, #13705, #9477, .T. ) ;
#4039=LINE ( 'NONE', #11648, #32 ) ;
#4050=PRODUCT_DEFINITION_CONTEXT ( 'detailed design', #8323, 'design' ) ;
#4087=ADVANCED_FACE ( 'NONE', ( #513, #2769, #13281, #1689, #6594, #574, #9026, #1554 ), #3721, .T. ) ;
#4111=AXIS2_PLACEMENT_3D ( 'NONE', #7501, #12006, #9985 ) ;
#4183=CIRCLE ( 'NONE', #9750, 1.999999999999996669 ) ;
#4211=DIRECTION ( 'NONE',  ( 1.000000000000000000, 0.000000000000000000, 0.000000000000000000 ) ) ;
#4221=ORIENTED_EDGE ( 'NONE', *, *, #10411, .F. ) ;
#4353=EDGE_CURVE ( 'NONE', #7731, #13005, #1185, .T. ) ;
#4391=DIRECTION ( 'NONE',  ( 1.000000000000000000, 0.000000000000000000, 0.000000000000000000 ) ) ;
#4393=EDGE_CURVE ( 'NONE', #8669, #189, #10302, .T. ) ;
#4398=CARTESIAN_POINT ( 'NONE',  ( 7.640422211807137209, 16.89844320975774750, 7.000000000000000000 ) ) ;
#4406=CARTESIAN_POINT ( 'NONE',  ( 0.000000000000000000, 0.000000000000000000, 0.000000000000000000 ) ) ;
#4480=DIRECTION ( 'NONE',  ( -0.000000000000000000, -0.000000000000000000, 1.000000000000000000 ) ) ;
#4507=CIRCLE ( 'NONE', #12508, 1.999999999999991340 ) ;
#4512=MANIFOLD_SOLID_BREP ( 'Cut-Extrude2', #9488 ) ;
#4517=DIRECTION ( 'NONE',  ( -1.000000000000000000, 0.000000000000000000, 0.000000000000000000 ) ) ;
#4526=( NAMED_UNIT ( * ) PLANE_ANGLE_UNIT ( ) SI_UNIT ( $, .RADIAN. ) );
#4527=CIRCLE ( 'NONE', #11657, 1.999999999999995781 ) ;
#4533=EDGE_LOOP ( 'NONE', ( #10333, #10689, #2538, #353 ) ) ;
#4535=DIRECTION ( 'NONE',  ( 1.000000000000000000, 0.000000000000000000, 0.000000000000000000 ) ) ;
#4553=CYLINDRICAL_SURFACE ( 'NONE', #1532, 1.999999999999996669 ) ;
#4568=DIRECTION ( 'NONE',  ( -0.000000000000000000, -0.000000000000000000, 1.000000000000000000 ) ) ;
#4573=ADVANCED_FACE ( 'NONE', ( #622 ), #1963, .F. ) ;
#4586=DIRECTION ( 'NONE',  ( -1.000000000000000000, 0.000000000000000000, 0.000000000000000000 ) ) ;
#4588=ORIENTED_EDGE ( 'NONE', *, *, #9233, .T. ) ;
#4630=ORIENTED_EDGE ( 'NONE', *, *, #5690, .T. ) ;
#4634=CARTESIAN_POINT ( 'NONE',  ( -18.45469220996244886, -1.832421873814834123, 0.000000000000000000 ) ) ;
#4643=EDGE_CURVE ( 'NONE', #4661, #7731, #4951, .T. ) ;
#4660=( LENGTH_UNIT ( ) NAMED_UNIT ( * ) SI_UNIT ( .MILLI., .METRE. ) );
#4661=VERTEX_POINT ( 'NONE', #8511 ) ;
#4665=AXIS2_PLACEMENT_3D ( 'NONE', #10191, #6893, #7936 ) ;
#4676=ORIENTED_EDGE ( 'NONE', *, *, #1249, .T. ) ;
#4726=AXIS2_PLACEMENT_3D ( 'NONE', #991, #1251, #3441 ) ;
#4737=DIRECTION ( 'NONE',  ( -0.000000000000000000, -0.000000000000000000, 1.000000000000000000 ) ) ;
#4751=ADVANCED_FACE ( 'NONE', ( #13112 ), #9000, .F. ) ;
#4856=DIRECTION ( 'NONE',  ( 1.000000000000000000, 0.000000000000000000, 0.000000000000000000 ) ) ;
#4877=LINE ( 'NONE', #10456, #7314 ) ;
#4889=ORIENTED_EDGE ( 'NONE', *, *, #381, .F. ) ;
#4908=CARTESIAN_POINT ( 'NONE',  ( -12.81426999815532497, 15.06602133594271820, 0.000000000000000000 ) ) ;
#4921=AXIS2_PLACEMENT_3D ( 'NONE', #9456, #13, #3185 ) ;
#4951=CIRCLE ( 'NONE', #9191, 6.000000000000000888 ) ;
#4955=ORIENTED_EDGE ( 'NONE', *, *, #11492, .T. ) ;
#4966=VECTOR ( 'NONE', #4568, 1000.000000000000000 ) ;
#5008=DIRECTION ( 'NONE',  ( 1.000000000000000000, 0.000000000000000000, 0.000000000000000000 ) ) ;
#5011=EDGE_CURVE ( 'NONE', #2929, #3628, #4527, .T. ) ;
#5019=FACE_OUTER_BOUND ( 'NONE', #1711, .T. ) ;
#5022=CIRCLE ( 'NONE', #13717, 1.999999999999993117 ) ;
#5046=AXIS2_PLACEMENT_3D ( 'NONE', #8307, #7106, #9224 ) ;
#5089=( NAMED_UNIT ( * ) SI_UNIT ( $, .STERADIAN. ) SOLID_ANGLE_UNIT ( ) );
#5111=CARTESIAN_POINT ( 'NONE',  ( -5.640422211807260666, -16.89844320975769776, 0.000000000000000000 ) ) ;
#5113=DIRECTION ( 'NONE',  ( 1.000000000000000000, 0.000000000000000000, 0.000000000000000000 ) ) ;
#5120=EDGE_LOOP ( 'NONE', ( #3154, #1025, #1155, #5726 ) ) ;
#5121=EDGE_CURVE ( 'NONE', #973, #12867, #13658, .T. ) ;
#5123=AXIS2_PLACEMENT_3D ( 'NONE', #1502, #329, #4586 ) ;
#5127=CARTESIAN_POINT ( 'NONE',  ( 24.03999999999999915, 2.944050905150237001E-15, 7.000000000000000000 ) ) ;
#5136=CARTESIAN_POINT ( 'NONE',  ( -10.81426999815532852, 15.06602133594271820, 7.000000000000000000 ) ) ;
#5139=CARTESIAN_POINT ( 'NONE',  ( -24.03999999999999915, 0.000000000000000000, 0.000000000000000000 ) ) ;
#5230=EDGE_CURVE ( 'NONE', #13004, #12299, #295, .T. ) ;
#5281=CARTESIAN_POINT ( 'NONE',  ( -7.640422211807256225, -16.89844320975769776, 0.000000000000000000 ) ) ;
#5297=AXIS2_PLACEMENT_3D ( 'NONE', #4398, #10825, #2175 ) ;
#5399=CIRCLE ( 'NONE', #3201, 24.03999999999999915 ) ;
#5407=EDGE_CURVE ( 'NONE', #9458, #7458, #5399, .T. ) ;
#5415=CIRCLE ( 'NONE', #9893, 1.999999999999995781 ) ;
#5421=FACE_BOUND ( 'NONE', #13491, .T. ) ;
#5430=ADVANCED_FACE ( 'NONE', ( #867 ), #3197, .F. ) ;
#5431=DIRECTION ( 'NONE',  ( 1.000000000000000000, 0.000000000000000000, 0.000000000000000000 ) ) ;
#5478=EDGE_CURVE ( 'NONE', #9008, #9150, #1272, .T. ) ;
#5481=PLANE ( 'NONE',  #9949 ) ;
#5544=DIRECTION ( 'NONE',  ( 1.000000000000000000, 0.000000000000000000, -0.000000000000000000 ) ) ;
#5562=CARTESIAN_POINT ( 'NONE',  ( 0.000000000000000000, 0.000000000000000000, 7.000000000000000000 ) ) ;
#5570=DIRECTION ( 'NONE',  ( 0.000000000000000000, 0.000000000000000000, 1.000000000000000000 ) ) ;
#5580=FACE_OUTER_BOUND ( 'NONE', #12599, .T. ) ;
#5584=VECTOR ( 'NONE', #1017, 1000.000000000000000 ) ;
#5690=EDGE_CURVE ( 'NONE', #10270, #12491, #5415, .T. ) ;
#5695=DIRECTION ( 'NONE',  ( -0.000000000000000000, -0.000000000000000000, 1.000000000000000000 ) ) ;
#5701=DIRECTION ( 'NONE',  ( -0.000000000000000000, -0.000000000000000000, 1.000000000000000000 ) ) ;
#5710=ADVANCED_FACE ( 'NONE', ( #9706 ), #6556, .F. ) ;
#5711=ORIENTED_EDGE ( 'NONE', *, *, #12535, .T. ) ;
#5716=DIRECTION ( 'NONE',  ( -0.000000000000000000, -0.000000000000000000, 1.000000000000000000 ) ) ;
#5726=ORIENTED_EDGE ( 'NONE', *, *, #3672, .F. ) ;
#5746=CIRCLE ( 'NONE', #13564, 1.999999999999996669 ) ;
#5762=ORIENTED_EDGE ( 'NONE', *, *, #11947, .F. ) ;
#5793=EDGE_CURVE ( 'NONE', #11959, #9990, #9667, .T. ) ;
#5830=( NAMED_UNIT ( * ) SI_UNIT ( $, .STERADIAN. ) SOLID_ANGLE_UNIT ( ) );
#5832=EDGE_CURVE ( 'NONE', #11639, #9038, #13019, .T. ) ;
#5852=EDGE_CURVE ( 'NONE', #1, #13705, #11682, .T. ) ;
#5931=EDGE_LOOP ( 'NONE', ( #249, #13160, #8482, #298 ) ) ;
#5938=DIRECTION ( 'NONE',  ( 0.000000000000000000, 0.000000000000000000, 1.000000000000000000 ) ) ;
#5980=AXIS2_PLACEMENT_3D ( 'NONE', #4406, #11300, #2663 ) ;
#5984=EDGE_CURVE ( 'NONE', #12154, #7369, #12132, .T. ) ;
#5990=ORIENTED_EDGE ( 'NONE', *, *, #5407, .T. ) ;
#6062=CYLINDRICAL_SURFACE ( 'NONE', #5046, 1.999999999999996669 ) ;
#6227=CARTESIAN_POINT ( 'NONE',  ( 10.81426999815522549, -15.06602133594279991, 0.000000000000000000 ) ) ;
#6244=DIRECTION ( 'NONE',  ( -0.000000000000000000, -0.000000000000000000, 1.000000000000000000 ) ) ;
#6253=ORIENTED_EDGE ( 'NONE', *, *, #2617, .T. ) ;
#6255=CARTESIAN_POINT ( 'NONE',  ( 9.640422211807132769, 16.89844320975774750, 7.000000000000000000 ) ) ;
#6280=ORIENTED_EDGE ( 'NONE', *, *, #5690, .F. ) ;
#6316=CARTESIAN_POINT ( 'NONE',  ( 18.45469220996244886, 1.832421873814834123, -3.000000000000000000 ) ) ;
#6383=ADVANCED_FACE ( 'NONE', ( #2581 ), #11083, .T. ) ;
#6407=DIRECTION ( 'NONE',  ( 0.000000000000000000, 0.000000000000000000, 1.000000000000000000 ) ) ;
#6434=AXIS2_PLACEMENT_3D ( 'NONE', #11654, #12825, #11856 ) ;
#6454=CARTESIAN_POINT ( 'NONE',  ( 12.81426999815521839, -15.06602133594279991, -3.000000000000000000 ) ) ;
#6478=AXIS2_PLACEMENT_3D ( 'NONE', #3582, #6708, #356 ) ;
#6480=AXIS2_PLACEMENT_3D ( 'NONE', #1693, #5938, #10228 ) ;
#6514=ORIENTED_EDGE ( 'NONE', *, *, #4643, .T. ) ;
#6541=CYLINDRICAL_SURFACE ( 'NONE', #6662, 1.999999999999996669 ) ;
#6547=FACE_BOUND ( 'NONE', #7647, .T. ) ;
#6556=CYLINDRICAL_SURFACE ( 'NONE', #7866, 6.000000000000000888 ) ;
#6572=ORIENTED_EDGE ( 'NONE', *, *, #10585, .F. ) ;
#6594=FACE_BOUND ( 'NONE', #1948, .T. ) ;
#6604=EDGE_CURVE ( 'NONE', #7369, #1, #2012, .T. ) ;
#6661=CIRCLE ( 'NONE', #9797, 1.999999999999994893 ) ;
#6662=AXIS2_PLACEMENT_3D ( 'NONE', #12694, #9623, #3334 ) ;
#6685=ORIENTED_EDGE ( 'NONE', *, *, #12535, .F. ) ;
#6698=VECTOR ( 'NONE', #5695, 1000.000000000000000 ) ;
#6708=DIRECTION ( 'NONE',  ( -0.000000000000000000, -0.000000000000000000, 1.000000000000000000 ) ) ;
#6714=CIRCLE ( 'NONE', #8729, 1.999999999999996669 ) ;
#6719=COLOUR_RGB ( '', 0.72549020, 0.75294118, 0.79215686) ;
#6731=EDGE_LOOP ( 'NONE', ( #8038, #12339 ) ) ;
#6770=EDGE_CURVE ( 'NONE', #973, #51, #1352, .T. ) ;
#6893=DIRECTION ( 'NONE',  ( 0.000000000000000000, 0.000000000000000000, 1.000000000000000000 ) ) ;
#6901=ORIENTED_EDGE ( 'NONE', *, *, #7381, .F. ) ;
#6917=ORIENTED_EDGE ( 'NONE', *, *, #8087, .T. ) ;
#6932=CARTESIAN_POINT ( 'NONE',  ( -5.640422211807260666, -16.89844320975769776, 7.000000000000000000 ) ) ;
#6946=VECTOR ( 'NONE', #13012, 1000.000000000000000 ) ;
#6958=DIRECTION ( 'NONE',  ( -0.000000000000000000, -0.000000000000000000, 1.000000000000000000 ) ) ;
#6989=ORIENTED_EDGE ( 'NONE', *, *, #5832, .T. ) ;
#7017=ORIENTED_EDGE ( 'NONE', *, *, #2311, .F. ) ;
#7039=CARTESIAN_POINT ( 'NONE',  ( -8.814269998155332075, 15.06602133594271820, -3.000000000000000000 ) ) ;
#7066=AXIS2_PLACEMENT_3D ( 'NONE', #7496, #6407, #10888 ) ;
#7080=EDGE_CURVE ( 'NONE', #12066, #13005, #8479, .T. ) ;
#7097=CIRCLE ( 'NONE', #9331, 1.999999999999991340 ) ;
#7106=DIRECTION ( 'NONE',  ( -0.000000000000000000, -0.000000000000000000, 1.000000000000000000 ) ) ;
#7128=DIRECTION ( 'NONE',  ( 1.000000000000000000, 0.000000000000000000, 0.000000000000000000 ) ) ;
#7211=FACE_OUTER_BOUND ( 'NONE', #5120, .T. ) ;
#7227=DIRECTION ( 'NONE',  ( 1.000000000000000000, 0.000000000000000000, 0.000000000000000000 ) ) ;
#7234=ORIENTED_EDGE ( 'NONE', *, *, #7880, .F. ) ;
#7240=CARTESIAN_POINT ( 'NONE',  ( -6.000000000000000888, 7.347880794884120722E-16, 7.000000000000000000 ) ) ;
#7258=DIRECTION ( 'NONE',  ( 0.000000000000000000, 0.000000000000000000, 1.000000000000000000 ) ) ;
#7271=CARTESIAN_POINT ( 'NONE',  ( 0.000000000000000000, 0.000000000000000000, 0.000000000000000000 ) ) ;
#7273=DIRECTION ( 'NONE',  ( -0.000000000000000000, -0.000000000000000000, 1.000000000000000000 ) ) ;
#7290=DIRECTION ( 'NONE',  ( 1.000000000000000000, 0.000000000000000000, 0.000000000000000000 ) ) ;
#7314=VECTOR ( 'NONE', #11438, 1000.000000000000000 ) ;
#7341=CARTESIAN_POINT ( 'NONE',  ( 7.640422211807137209, 16.89844320975774750, 7.000000000000000000 ) ) ;
#7358=CARTESIAN_POINT ( 'NONE',  ( 7.640422211807137209, 16.89844320975774750, 0.000000000000000000 ) ) ;
#7369=VERTEX_POINT ( 'NONE', #8032 ) ;
#7379=AXIS2_PLACEMENT_3D ( 'NONE', #13252, #1515, #1592 ) ;
#7381=EDGE_CURVE ( 'NONE', #3628, #2929, #12163, .T. ) ;
#7420=CARTESIAN_POINT ( 'NONE',  ( 8.814269998155230823, -15.06602133594279991, -3.000000000000000000 ) ) ;
#7458=VERTEX_POINT ( 'NONE', #3514 ) ;
#7496=CARTESIAN_POINT ( 'NONE',  ( -18.45469220996244886, -1.832421873814834123, 7.000000000000000000 ) ) ;
#7501=CARTESIAN_POINT ( 'NONE',  ( 18.45469220996244886, 1.832421873814834123, 7.000000000000000000 ) ) ;
#7526=CIRCLE ( 'NONE', #2679, 1.999999999999996669 ) ;
#7549=CIRCLE ( 'NONE', #3785, 1.999999999999993117 ) ;
#7640=DIRECTION ( 'NONE',  ( 0.000000000000000000, 0.000000000000000000, 1.000000000000000000 ) ) ;
#7647=EDGE_LOOP ( 'NONE', ( #4630, #6917 ) ) ;
#7652=DIRECTION ( 'NONE',  ( 0.000000000000000000, 0.000000000000000000, 1.000000000000000000 ) ) ;
#7710=ORIENTED_EDGE ( 'NONE', *, *, #2987, .F. ) ;
#7731=VERTEX_POINT ( 'NONE', #12218 ) ;
#7768=CIRCLE ( 'NONE', #4665, 24.03999999999999915 ) ;
#7817=DIRECTION ( 'NONE',  ( 1.000000000000000000, 0.000000000000000000, 0.000000000000000000 ) ) ;
#7866=AXIS2_PLACEMENT_3D ( 'NONE', #1317, #3287, #2395 ) ;
#7873=CARTESIAN_POINT ( 'NONE',  ( 8.814269998155230823, -15.06602133594279991, 7.000000000000000000 ) ) ;
#7880=EDGE_CURVE ( 'NONE', #13705, #1, #5022, .T. ) ;
#7898=ADVANCED_BREP_SHAPE_REPRESENTATION ( '', ( #4512, #6434 ), #2686 ) ;
#7936=DIRECTION ( 'NONE',  ( 1.000000000000000000, 0.000000000000000000, 0.000000000000000000 ) ) ;
#7948=EDGE_LOOP ( 'NONE', ( #2953, #12990, #10761, #8703 ) ) ;
#7985=ORIENTED_EDGE ( 'NONE', *, *, #2617, .F. ) ;
#8032=CARTESIAN_POINT ( 'NONE',  ( 12.81426999815521839, -15.06602133594279991, 0.000000000000000000 ) ) ;
#8038=ORIENTED_EDGE ( 'NONE', *, *, #12475, .F. ) ;
#8046=ADVANCED_FACE ( 'NONE', ( #10603, #11928, #6547, #10747, #5421, #3219, #8434, #10814 ), #5481, .F. ) ;
#8087=EDGE_CURVE ( 'NONE', #12491, #10270, #12826, .T. ) ;
#8105=CARTESIAN_POINT ( 'NONE',  ( 8.814269998155230823, -15.06602133594279991, 0.000000000000000000 ) ) ;
#8134=DIRECTION ( 'NONE',  ( -0.000000000000000000, -0.000000000000000000, 1.000000000000000000 ) ) ;
#8172=ADVANCED_FACE ( 'NONE', ( #11091 ), #8784, .F. ) ;
#8182=EDGE_LOOP ( 'NONE', ( #220, #9104 ) ) ;
#8188=EDGE_CURVE ( 'NONE', #9150, #9852, #11956, .T. ) ;
#8190=CIRCLE ( 'NONE', #7066, 1.999999999999991340 ) ;
#8234=ORIENTED_EDGE ( 'NONE', *, *, #10585, .T. ) ;
#8307=CARTESIAN_POINT ( 'NONE',  ( 7.640422211807137209, 16.89844320975774750, -3.000000000000000000 ) ) ;
#8310=( LENGTH_UNIT ( ) NAMED_UNIT ( * ) SI_UNIT ( .MILLI., .METRE. ) );
#8323=APPLICATION_CONTEXT ( 'automotive_design' ) ;
#8332=DIRECTION ( 'NONE',  ( 1.000000000000000000, 0.000000000000000000, 0.000000000000000000 ) ) ;
#8336=AXIS2_PLACEMENT_3D ( 'NONE', #9061, #5570, #7227 ) ;
#8358=DIRECTION ( 'NONE',  ( 0.000000000000000000, 0.000000000000000000, 1.000000000000000000 ) ) ;
#8414=ORIENTED_EDGE ( 'NONE', *, *, #36, .T. ) ;
#8434=FACE_BOUND ( 'NONE', #12197, .T. ) ;
#8479=CIRCLE ( 'NONE', #4921, 6.000000000000000888 ) ;
#8482=ORIENTED_EDGE ( 'NONE', *, *, #6770, .T. ) ;
#8511=CARTESIAN_POINT ( 'NONE',  ( -6.000000000000000888, 7.347880794884120722E-16, 0.000000000000000000 ) ) ;
#8539=LINE ( 'NONE', #8677, #9777 ) ;
#8560=DIRECTION ( 'NONE',  ( 1.000000000000000000, 0.000000000000000000, 0.000000000000000000 ) ) ;
#8569=EDGE_LOOP ( 'NONE', ( #12137, #2418 ) ) ;
#8638=PRODUCT_DEFINITION_SHAPE ( 'NONE', 'NONE',  #566 ) ;
#8669=VERTEX_POINT ( 'NONE', #11076 ) ;
#8677=CARTESIAN_POINT ( 'NONE',  ( -24.03999999999999915, 0.000000000000000000, 7.000000000000000000 ) ) ;
#8703=ORIENTED_EDGE ( 'NONE', *, *, #6604, .F. ) ;
#8729=AXIS2_PLACEMENT_3D ( 'NONE', #1089, #7640, #8560 ) ;
#8734=MECHANICAL_DESIGN_GEOMETRIC_PRESENTATION_REPRESENTATION('',(#9412),#255);
#8739=AXIS2_PLACEMENT_3D ( 'NONE', #7341, #11631, #12401 ) ;
#8756=CARTESIAN_POINT ( 'NONE',  ( 20.45469220996244175, 1.832421873814834123, -3.000000000000000000 ) ) ;
#8762=ORIENTED_EDGE ( 'NONE', *, *, #5832, .F. ) ;
#8784=CYLINDRICAL_SURFACE ( 'NONE', #10618, 6.000000000000000888 ) ;
#8819=FACE_OUTER_BOUND ( 'NONE', #12135, .T. ) ;
#8837=CARTESIAN_POINT ( 'NONE',  ( 5.640422211807141650, 16.89844320975774750, 0.000000000000000000 ) ) ;
#8901=ORIENTED_EDGE ( 'NONE', *, *, #4393, .T. ) ;
#8904=ORIENTED_EDGE ( 'NONE', *, *, #12720, .F. ) ;
#8911=ORIENTED_EDGE ( 'NONE', *, *, #5230, .F. ) ;
#8924=EDGE_LOOP ( 'NONE', ( #8911, #9821, #11246, #10465 ) ) ;
#8925=CARTESIAN_POINT ( 'NONE',  ( -16.45469220996245596, -1.832421873814834123, -3.000000000000000000 ) ) ;
#9000=CYLINDRICAL_SURFACE ( 'NONE', #7379, 1.999999999999995781 ) ;
#9008=VERTEX_POINT ( 'NONE', #2545 ) ;
#9026=FACE_BOUND ( 'NONE', #12336, .T. ) ;
#9038=VERTEX_POINT ( 'NONE', #1672 ) ;
#9061=CARTESIAN_POINT ( 'NONE',  ( 10.81426999815522549, -15.06602133594279991, 0.000000000000000000 ) ) ;
#9104=ORIENTED_EDGE ( 'NONE', *, *, #2700, .F. ) ;
#9105=ADVANCED_FACE ( 'NONE', ( #5019 ), #6062, .F. ) ;
#9121=PRODUCT_DEFINITION_FORMATION_WITH_SPECIFIED_SOURCE ( 'ANY', '', #10774, .NOT_KNOWN. ) ;
#9142=ORIENTED_EDGE ( 'NONE', *, *, #5478, .F. ) ;
#9150=VERTEX_POINT ( 'NONE', #3981 ) ;
#9179=DIRECTION ( 'NONE',  ( -0.000000000000000000, -0.000000000000000000, 1.000000000000000000 ) ) ;
#9191=AXIS2_PLACEMENT_3D ( 'NONE', #120, #10548, #2108 ) ;
#9224=DIRECTION ( 'NONE',  ( 1.000000000000000000, 0.000000000000000000, 0.000000000000000000 ) ) ;
#9233=EDGE_CURVE ( 'NONE', #9852, #9150, #8190, .T. ) ;
#9253=EDGE_CURVE ( 'NONE', #13005, #12066, #10419, .T. ) ;
#9331=AXIS2_PLACEMENT_3D ( 'NONE', #12383, #10156, #12107 ) ;
#9412=STYLED_ITEM ( 'NONE', ( #11383 ), #4512 ) ;
#9420=CARTESIAN_POINT ( 'NONE',  ( -7.640422211807256225, -16.89844320975769776, 7.000000000000000000 ) ) ;
#9456=CARTESIAN_POINT ( 'NONE',  ( 0.000000000000000000, 0.000000000000000000, 7.000000000000000000 ) ) ;
#9458=VERTEX_POINT ( 'NONE', #5139 ) ;
#9477=LINE ( 'NONE', #7420, #5584 ) ;
#9488=CLOSED_SHELL ( 'NONE', ( #12668, #2580, #4751, #5430, #11208, #9105, #5710, #9769, #6383, #4087, #8046, #8172, #11815, #2148, #1582, #3327, #4573, #492 ) ) ;
#9516=EDGE_LOOP ( 'NONE', ( #775, #7234 ) ) ;
#9558=DIRECTION ( 'NONE',  ( 1.000000000000000000, 0.000000000000000000, 0.000000000000000000 ) ) ;
#9592=ORIENTED_EDGE ( 'NONE', *, *, #2992, .T. ) ;
#9618=DIRECTION ( 'NONE',  ( 1.000000000000000000, 0.000000000000000000, 0.000000000000000000 ) ) ;
#9623=DIRECTION ( 'NONE',  ( -0.000000000000000000, -0.000000000000000000, 1.000000000000000000 ) ) ;
#9637=ORIENTED_EDGE ( 'NONE', *, *, #11492, .F. ) ;
#9646=AXIS2_PLACEMENT_3D ( 'NONE', #7358, #1154, #11650 ) ;
#9666=ORIENTED_EDGE ( 'NONE', *, *, #5011, .F. ) ;
#9667=CIRCLE ( 'NONE', #11447, 1.999999999999994893 ) ;
#9706=FACE_OUTER_BOUND ( 'NONE', #4533, .T. ) ;
#9717=CARTESIAN_POINT ( 'NONE',  ( 6.000000000000000888, 0.000000000000000000, -43.00000000000000000 ) ) ;
#9732=ORIENTED_EDGE ( 'NONE', *, *, #5793, .T. ) ;
#9748=APPLICATION_CONTEXT ( 'automotive_design' ) ;
#9750=AXIS2_PLACEMENT_3D ( 'NONE', #5136, #2934, #11569 ) ;
#9759=CARTESIAN_POINT ( 'NONE',  ( 0.000000000000000000, 0.000000000000000000, 0.000000000000000000 ) ) ;
#9769=ADVANCED_FACE ( 'NONE', ( #9830 ), #12188, .T. ) ;
#9777=VECTOR ( 'NONE', #1268, 1000.000000000000000 ) ;
#9779=UNCERTAINTY_MEASURE_WITH_UNIT (LENGTH_MEASURE( 1.000000000000000082E-05 ), #8310, 'distance_accuracy_value', 'NONE');
#9790=ORIENTED_EDGE ( 'NONE', *, *, #7080, .F. ) ;
#9797=AXIS2_PLACEMENT_3D ( 'NONE', #13334, #12306, #13206 ) ;
#9805=EDGE_LOOP ( 'NONE', ( #13484, #5711, #10397, #976 ) ) ;
#9821=ORIENTED_EDGE ( 'NONE', *, *, #12720, .T. ) ;
#9823=ORIENTED_EDGE ( 'NONE', *, *, #1683, .T. ) ;
#9830=FACE_OUTER_BOUND ( 'NONE', #8924, .T. ) ;
#9845=EDGE_LOOP ( 'NONE', ( #6685, #5762, #9823, #6989 ) ) ;
#9852=VERTEX_POINT ( 'NONE', #13441 ) ;
#9869=AXIS2_PLACEMENT_3D ( 'NONE', #442, #11004, #12039 ) ;
#9893=AXIS2_PLACEMENT_3D ( 'NONE', #12984, #1986, #5431 ) ;
#9910=ORIENTED_EDGE ( 'NONE', *, *, #12475, .T. ) ;
#9930=FILL_AREA_STYLE ('',( #2474 ) ) ;
#9949=AXIS2_PLACEMENT_3D ( 'NONE', #9759, #184, #12971 ) ;
#9985=DIRECTION ( 'NONE',  ( 1.000000000000000000, 0.000000000000000000, 0.000000000000000000 ) ) ;
#9990=VERTEX_POINT ( 'NONE', #13707 ) ;
#10048=CARTESIAN_POINT ( 'NONE',  ( 0.000000000000000000, 0.000000000000000000, -43.00000000000000000 ) ) ;
#10059=CARTESIAN_POINT ( 'NONE',  ( -12.81426999815532497, 15.06602133594271820, -3.000000000000000000 ) ) ;
#10085=VECTOR ( 'NONE', #3238, 1000.000000000000000 ) ;
#10091=CARTESIAN_POINT ( 'NONE',  ( 0.000000000000000000, 0.000000000000000000, 7.000000000000000000 ) ) ;
#10156=DIRECTION ( 'NONE',  ( 0.000000000000000000, 0.000000000000000000, 1.000000000000000000 ) ) ;
#10191=CARTESIAN_POINT ( 'NONE',  ( 0.000000000000000000, 0.000000000000000000, 0.000000000000000000 ) ) ;
#10228=DIRECTION ( 'NONE',  ( 1.000000000000000000, 0.000000000000000000, 0.000000000000000000 ) ) ;
#10236=ORIENTED_EDGE ( 'NONE', *, *, #9233, .F. ) ;
#10268=VECTOR ( 'NONE', #9179, 1000.000000000000000 ) ;
#10270=VERTEX_POINT ( 'NONE', #5111 ) ;
#10271=AXIS2_PLACEMENT_3D ( 'NONE', #13136, #3585, #7817 ) ;
#10299=CARTESIAN_POINT ( 'NONE',  ( -6.000000000000000888, 7.347880794884120722E-16, -43.00000000000000000 ) ) ;
#10302=CIRCLE ( 'NONE', #4726, 1.999999999999996669 ) ;
#10333=ORIENTED_EDGE ( 'NONE', *, *, #4643, .F. ) ;
#10375=EDGE_LOOP ( 'NONE', ( #7017, #1265, #8414, #1896 ) ) ;
#10397=ORIENTED_EDGE ( 'NONE', *, *, #1830, .T. ) ;
#10402=DIRECTION ( 'NONE',  ( -0.000000000000000000, -0.000000000000000000, 1.000000000000000000 ) ) ;
#10411=EDGE_CURVE ( 'NONE', #12867, #973, #7526, .T. ) ;
#10419=CIRCLE ( 'NONE', #1048, 6.000000000000000888 ) ;
#10456=CARTESIAN_POINT ( 'NONE',  ( 16.45469220996245241, 1.832421873814834345, -3.000000000000000000 ) ) ;
#10465=ORIENTED_EDGE ( 'NONE', *, *, #11390, .F. ) ;
#10489=VERTEX_POINT ( 'NONE', #10698 ) ;
#10548=DIRECTION ( 'NONE',  ( 0.000000000000000000, 0.000000000000000000, 1.000000000000000000 ) ) ;
#10585=EDGE_CURVE ( 'NONE', #7731, #4661, #3769, .T. ) ;
#10592=VERTEX_POINT ( 'NONE', #11236 ) ;
#10599=EDGE_CURVE ( 'NONE', #7458, #9458, #7768, .T. ) ;
#10603=FACE_BOUND ( 'NONE', #3560, .T. ) ;
#10618=AXIS2_PLACEMENT_3D ( 'NONE', #10048, #4737, #3556 ) ;
#10626=CARTESIAN_POINT ( 'NONE',  ( 7.640422211807137209, 16.89844320975774750, -3.000000000000000000 ) ) ;
#10627=DIRECTION ( 'NONE',  ( 0.000000000000000000, 0.000000000000000000, 1.000000000000000000 ) ) ;
#10689=ORIENTED_EDGE ( 'NONE', *, *, #2987, .T. ) ;
#10698=CARTESIAN_POINT ( 'NONE',  ( -8.814269998155332075, 15.06602133594271820, 7.000000000000000000 ) ) ;
#10732=AXIS2_PLACEMENT_3D ( 'NONE', #191, #3489, #4391 ) ;
#10747=FACE_BOUND ( 'NONE', #13345, .T. ) ;
#10761=ORIENTED_EDGE ( 'NONE', *, *, #7880, .T. ) ;
#10774=PRODUCT ( 'Rotary Faceplate', 'Rotary Faceplate', '', ( #11358 ) ) ;
#10814=FACE_OUTER_BOUND ( 'NONE', #8569, .T. ) ;
#10825=DIRECTION ( 'NONE',  ( 0.000000000000000000, 0.000000000000000000, 1.000000000000000000 ) ) ;
#10862=ORIENTED_EDGE ( 'NONE', *, *, #5121, .T. ) ;
#10888=DIRECTION ( 'NONE',  ( 1.000000000000000000, 0.000000000000000000, 0.000000000000000000 ) ) ;
#10972=CARTESIAN_POINT ( 'NONE',  ( -9.640422211807251784, -16.89844320975769776, 7.000000000000000000 ) ) ;
#10992=FACE_OUTER_BOUND ( 'NONE', #11719, .T. ) ;
#11004=DIRECTION ( 'NONE',  ( -0.000000000000000000, -0.000000000000000000, 1.000000000000000000 ) ) ;
#11036=LINE ( 'NONE', #10059, #3110 ) ;
#11047=SURFACE_SIDE_STYLE ('',( #2547 ) ) ;
#11065=CYLINDRICAL_SURFACE ( 'NONE', #9869, 1.999999999999993117 ) ;
#11076=CARTESIAN_POINT ( 'NONE',  ( -8.814269998155332075, 15.06602133594271820, 0.000000000000000000 ) ) ;
#11083=CYLINDRICAL_SURFACE ( 'NONE', #5123, 24.03999999999999915 ) ;
#11091=FACE_OUTER_BOUND ( 'NONE', #13037, .T. ) ;
#11116=CARTESIAN_POINT ( 'NONE',  ( -7.640422211807256225, -16.89844320975769776, 7.000000000000000000 ) ) ;
#11174=ORIENTED_EDGE ( 'NONE', *, *, #12420, .F. ) ;
#11208=ADVANCED_FACE ( 'NONE', ( #2865 ), #2734, .F. ) ;
#11232=DIRECTION ( 'NONE',  ( 1.000000000000000000, 0.000000000000000000, 0.000000000000000000 ) ) ;
#11236=CARTESIAN_POINT ( 'NONE',  ( -16.45469220996245596, -1.832421873814834123, 0.000000000000000000 ) ) ;
#11246=ORIENTED_EDGE ( 'NONE', *, *, #10599, .T. ) ;
#11300=DIRECTION ( 'NONE',  ( 0.000000000000000000, 0.000000000000000000, 1.000000000000000000 ) ) ;
#11322=ORIENTED_EDGE ( 'NONE', *, *, #982, .T. ) ;
#11358=PRODUCT_CONTEXT ( 'NONE', #9748, 'mechanical' ) ;
#11370=CARTESIAN_POINT ( 'NONE',  ( -9.640422211807251784, -16.89844320975769776, 0.000000000000000000 ) ) ;
#11383=PRESENTATION_STYLE_ASSIGNMENT (( #12430 ) ) ;
#11390=EDGE_CURVE ( 'NONE', #12299, #9458, #8539, .T. ) ;
#11414=ORIENTED_EDGE ( 'NONE', *, *, #9253, .T. ) ;
#11438=DIRECTION ( 'NONE',  ( -0.000000000000000000, -0.000000000000000000, 1.000000000000000000 ) ) ;
#11447=AXIS2_PLACEMENT_3D ( 'NONE', #11941, #4009, #5113 ) ;
#11465=CARTESIAN_POINT ( 'NONE',  ( -5.640422211807260666, -16.89844320975769776, -3.000000000000000000 ) ) ;
#11474=LINE ( 'NONE', #10299, #10268 ) ;
#11485=DIRECTION ( 'NONE',  ( 1.000000000000000000, 0.000000000000000000, 0.000000000000000000 ) ) ;
#11492=EDGE_CURVE ( 'NONE', #10592, #9008, #7097, .T. ) ;
#11494=AXIS2_PLACEMENT_3D ( 'NONE', #5281, #2383, #9558 ) ;
#11517=CARTESIAN_POINT ( 'NONE',  ( -12.81426999815532497, 15.06602133594271820, 7.000000000000000000 ) ) ;
#11555=CARTESIAN_POINT ( 'NONE',  ( -9.640422211807251784, -16.89844320975769776, -3.000000000000000000 ) ) ;
#11569=DIRECTION ( 'NONE',  ( 1.000000000000000000, 0.000000000000000000, 0.000000000000000000 ) ) ;
#11577=CARTESIAN_POINT ( 'NONE',  ( 24.03999999999999915, 2.944050905150237001E-15, 7.000000000000000000 ) ) ;
#11578=CARTESIAN_POINT ( 'NONE',  ( 18.45469220996244886, 1.832421873814834123, -3.000000000000000000 ) ) ;
#11612=VECTOR ( 'NONE', #6244, 1000.000000000000000 ) ;
#11631=DIRECTION ( 'NONE',  ( 0.000000000000000000, 0.000000000000000000, 1.000000000000000000 ) ) ;
#11639=VERTEX_POINT ( 'NONE', #12656 ) ;
#11648=CARTESIAN_POINT ( 'NONE',  ( 5.640422211807141650, 16.89844320975774750, -3.000000000000000000 ) ) ;
#11650=DIRECTION ( 'NONE',  ( 1.000000000000000000, 0.000000000000000000, 0.000000000000000000 ) ) ;
#11652=FACE_OUTER_BOUND ( 'NONE', #9845, .T. ) ;
#11654=CARTESIAN_POINT ( 'NONE',  ( 0.000000000000000000, 0.000000000000000000, 0.000000000000000000 ) ) ;
#11657=AXIS2_PLACEMENT_3D ( 'NONE', #9420, #8358, #9618 ) ;
#11680=FACE_OUTER_BOUND ( 'NONE', #5931, .T. ) ;
#11682=CIRCLE ( 'NONE', #3217, 1.999999999999993117 ) ;
#11691=ORIENTED_EDGE ( 'NONE', *, *, #5984, .T. ) ;
#11697=DIRECTION ( 'NONE',  ( 1.000000000000000000, 0.000000000000000000, 0.000000000000000000 ) ) ;
#11719=EDGE_LOOP ( 'NONE', ( #7985, #6280, #602, #12796 ) ) ;
#11756=DIRECTION ( 'NONE',  ( 1.000000000000000000, 0.000000000000000000, 0.000000000000000000 ) ) ;
#11804=CYLINDRICAL_SURFACE ( 'NONE', #6478, 1.999999999999996669 ) ;
#11815=ADVANCED_FACE ( 'NONE', ( #11680 ), #4553, .F. ) ;
#11856=DIRECTION ( 'NONE',  ( 1.000000000000000000, 0.000000000000000000, 0.000000000000000000 ) ) ;
#11861=VECTOR ( 'NONE', #8134, 1000.000000000000000 ) ;
#11895=ORIENTED_EDGE ( 'NONE', *, *, #4011, .F. ) ;
#11928=FACE_BOUND ( 'NONE', #1040, .T. ) ;
#11936=CARTESIAN_POINT ( 'NONE',  ( 9.640422211807132769, 16.89844320975774750, 0.000000000000000000 ) ) ;
#11941=CARTESIAN_POINT ( 'NONE',  ( 18.45469220996244886, 1.832421873814834123, 0.000000000000000000 ) ) ;
#11947=EDGE_CURVE ( 'NONE', #9990, #11959, #6661, .T. ) ;
#11956=CIRCLE ( 'NONE', #13513, 1.999999999999991340 ) ;
#11959=VERTEX_POINT ( 'NONE', #3709 ) ;
#11995=CARTESIAN_POINT ( 'NONE',  ( -18.45469220996244886, -1.832421873814834123, 7.000000000000000000 ) ) ;
#12006=DIRECTION ( 'NONE',  ( 0.000000000000000000, 0.000000000000000000, 1.000000000000000000 ) ) ;
#12038=ORIENTED_EDGE ( 'NONE', *, *, #11947, .T. ) ;
#12039=DIRECTION ( 'NONE',  ( 1.000000000000000000, 0.000000000000000000, 0.000000000000000000 ) ) ;
#12066=VERTEX_POINT ( 'NONE', #7240 ) ;
#12107=DIRECTION ( 'NONE',  ( 1.000000000000000000, 0.000000000000000000, 0.000000000000000000 ) ) ;
#12112=DIRECTION ( 'NONE',  ( 0.000000000000000000, 0.000000000000000000, 1.000000000000000000 ) ) ;
#12132=CIRCLE ( 'NONE', #8336, 1.999999999999993117 ) ;
#12135=EDGE_LOOP ( 'NONE', ( #11895, #13113, #2861, #2346 ) ) ;
#12137=ORIENTED_EDGE ( 'NONE', *, *, #5407, .F. ) ;
#12154=VERTEX_POINT ( 'NONE', #8105 ) ;
#12163=CIRCLE ( 'NONE', #1441, 1.999999999999995781 ) ;
#12188=CYLINDRICAL_SURFACE ( 'NONE', #3302, 24.03999999999999915 ) ;
#12197=EDGE_LOOP ( 'NONE', ( #8234, #6514 ) ) ;
#12218=CARTESIAN_POINT ( 'NONE',  ( 6.000000000000000888, 0.000000000000000000, 0.000000000000000000 ) ) ;
#12232=CIRCLE ( 'NONE', #5297, 1.999999999999996669 ) ;
#12299=VERTEX_POINT ( 'NONE', #1594 ) ;
#12306=DIRECTION ( 'NONE',  ( 0.000000000000000000, 0.000000000000000000, 1.000000000000000000 ) ) ;
#12336=EDGE_LOOP ( 'NONE', ( #1781, #9790 ) ) ;
#12339=ORIENTED_EDGE ( 'NONE', *, *, #36, .F. ) ;
#12369=CARTESIAN_POINT ( 'NONE',  ( -18.45469220996244886, -1.832421873814834123, -3.000000000000000000 ) ) ;
#12383=CARTESIAN_POINT ( 'NONE',  ( -18.45469220996244886, -1.832421873814834123, 0.000000000000000000 ) ) ;
#12401=DIRECTION ( 'NONE',  ( 1.000000000000000000, 0.000000000000000000, 0.000000000000000000 ) ) ;
#12420=EDGE_CURVE ( 'NONE', #189, #826, #11036, .T. ) ;
#12430=SURFACE_STYLE_USAGE ( .BOTH. , #11047 ) ;
#12436=ORIENTED_EDGE ( 'NONE', *, *, #8188, .F. ) ;
#12470=CYLINDRICAL_SURFACE ( 'NONE', #13414, 1.999999999999991340 ) ;
#12475=EDGE_CURVE ( 'NONE', #10489, #826, #5746, .T. ) ;
#12485=DIRECTION ( 'NONE',  ( -0.000000000000000000, -0.000000000000000000, 1.000000000000000000 ) ) ;
#12491=VERTEX_POINT ( 'NONE', #11370 ) ;
#12495=VECTOR ( 'NONE', #3462, 1000.000000000000000 ) ;
#12508=AXIS2_PLACEMENT_3D ( 'NONE', #4634, #12112, #7128 ) ;
#12515=AXIS2_PLACEMENT_3D ( 'NONE', #10091, #1288, #5544 ) ;
#12535=EDGE_CURVE ( 'NONE', #11959, #9038, #4877, .T. ) ;
#12599=EDGE_LOOP ( 'NONE', ( #11174, #1079, #13162, #9910 ) ) ;
#12656=CARTESIAN_POINT ( 'NONE',  ( 20.45469220996244175, 1.832421873814834123, 7.000000000000000000 ) ) ;
#12668=ADVANCED_FACE ( 'NONE', ( #2093 ), #6541, .F. ) ;
#12694=CARTESIAN_POINT ( 'NONE',  ( -10.81426999815532852, 15.06602133594271820, -3.000000000000000000 ) ) ;
#12719=ORIENTED_EDGE ( 'NONE', *, *, #6770, .F. ) ;
#12720=EDGE_CURVE ( 'NONE', #13004, #7458, #3411, .T. ) ;
#12743=ORIENTED_EDGE ( 'NONE', *, *, #1696, .T. ) ;
#12789=ORIENTED_EDGE ( 'NONE', *, *, #982, .F. ) ;
#12796=ORIENTED_EDGE ( 'NONE', *, *, #5011, .T. ) ;
#12806=DIRECTION ( 'NONE',  ( 0.000000000000000000, 0.000000000000000000, 1.000000000000000000 ) ) ;
#12825=DIRECTION ( 'NONE',  ( 0.000000000000000000, 0.000000000000000000, 1.000000000000000000 ) ) ;
#12826=CIRCLE ( 'NONE', #11494, 1.999999999999995781 ) ;
#12867=VERTEX_POINT ( 'NONE', #8837 ) ;
#12971=DIRECTION ( 'NONE',  ( 1.000000000000000000, 0.000000000000000000, -0.000000000000000000 ) ) ;
#12984=CARTESIAN_POINT ( 'NONE',  ( -7.640422211807256225, -16.89844320975769776, 0.000000000000000000 ) ) ;
#12987=ORIENTED_EDGE ( 'NONE', *, *, #8087, .F. ) ;
#12990=ORIENTED_EDGE ( 'NONE', *, *, #4011, .T. ) ;
#13004=VERTEX_POINT ( 'NONE', #5127 ) ;
#13005=VERTEX_POINT ( 'NONE', #3816 ) ;
#13012=DIRECTION ( 'NONE',  ( -0.000000000000000000, -0.000000000000000000, 1.000000000000000000 ) ) ;
#13019=CIRCLE ( 'NONE', #4111, 1.999999999999994893 ) ;
#13037=EDGE_LOOP ( 'NONE', ( #7710, #6572, #13620, #11414 ) ) ;
#13051=CARTESIAN_POINT ( 'NONE',  ( 10.81426999815522549, -15.06602133594279991, 7.000000000000000000 ) ) ;
#13068=ORIENTED_EDGE ( 'NONE', *, *, #3672, .T. ) ;
#13083=CARTESIAN_POINT ( 'NONE',  ( 9.640422211807132769, 16.89844320975774750, -3.000000000000000000 ) ) ;
#13112=FACE_OUTER_BOUND ( 'NONE', #3928, .T. ) ;
#13113=ORIENTED_EDGE ( 'NONE', *, *, #2992, .F. ) ;
#13136=CARTESIAN_POINT ( 'NONE',  ( -7.640422211807256225, -16.89844320975769776, -3.000000000000000000 ) ) ;
#13160=ORIENTED_EDGE ( 'NONE', *, *, #5121, .F. ) ;
#13162=ORIENTED_EDGE ( 'NONE', *, *, #562, .T. ) ;
#13206=DIRECTION ( 'NONE',  ( 1.000000000000000000, 0.000000000000000000, 0.000000000000000000 ) ) ;
#13252=CARTESIAN_POINT ( 'NONE',  ( -7.640422211807256225, -16.89844320975769776, -3.000000000000000000 ) ) ;
#13281=FACE_BOUND ( 'NONE', #3171, .T. ) ;
#13334=CARTESIAN_POINT ( 'NONE',  ( 18.45469220996244886, 1.832421873814834123, 0.000000000000000000 ) ) ;
#13337=DIRECTION ( 'NONE',  ( 0.000000000000000000, 0.000000000000000000, 1.000000000000000000 ) ) ;
#13345=EDGE_LOOP ( 'NONE', ( #9592, #11691 ) ) ;
#13403=CARTESIAN_POINT ( 'NONE',  ( 10.81426999815522549, -15.06602133594279991, 7.000000000000000000 ) ) ;
#13414=AXIS2_PLACEMENT_3D ( 'NONE', #3058, #7273, #11485 ) ;
#13441=CARTESIAN_POINT ( 'NONE',  ( -16.45469220996245596, -1.832421873814834123, 7.000000000000000000 ) ) ;
#13446=LINE ( 'NONE', #11555, #11861 ) ;
#13475=EDGE_CURVE ( 'NONE', #51, #1551, #12232, .T. ) ;
#13484=ORIENTED_EDGE ( 'NONE', *, *, #5793, .F. ) ;
#13491=EDGE_LOOP ( 'NONE', ( #12038, #9732 ) ) ;
#13513=AXIS2_PLACEMENT_3D ( 'NONE', #11995, #396, #3686 ) ;
#13564=AXIS2_PLACEMENT_3D ( 'NONE', #13591, #810, #5008 ) ;
#13591=CARTESIAN_POINT ( 'NONE',  ( -10.81426999815532852, 15.06602133594271820, 7.000000000000000000 ) ) ;
#13620=ORIENTED_EDGE ( 'NONE', *, *, #4353, .T. ) ;
#13650=CARTESIAN_POINT ( 'NONE',  ( 10.81426999815522549, -15.06602133594279991, -3.000000000000000000 ) ) ;
#13658=CIRCLE ( 'NONE', #9646, 1.999999999999996669 ) ;
#13691=LINE ( 'NONE', #11465, #2490 ) ;
#13705=VERTEX_POINT ( 'NONE', #7873 ) ;
#13707=CARTESIAN_POINT ( 'NONE',  ( 20.45469220996244175, 1.832421873814834123, 0.000000000000000000 ) ) ;
#13717=AXIS2_PLACEMENT_3D ( 'NONE', #13403, #2875, #3022 ) ;
#13792=DIRECTION ( 'NONE',  ( -0.000000000000000000, -0.000000000000000000, -1.000000000000000000 ) ) ;
ENDSEC;
END-ISO-10303-21;
